ISO-10303-21;
HEADER;
/* Generated by software containing ST-Developer
 * from STEP Tools, Inc. (www.steptools.com) 
 */

FILE_DESCRIPTION(
/* description */ ('Gauge isolation and snubber set'),
/* implementation_level */ '2;1');

FILE_NAME(
/* name */ 'Hex Bolt - M6 x 30 mm.step',
/* time_stamp */ '2026-10-29T16:58:15-07:00',
/* author */ (''),
/* organization */ (''),
/* preprocessor_version */ 'ST-DEVELOPER v20.2',
/* originating_system */ 'Autodesk Translation Framework v15.17.0.0',
/* authorisation */ '');

FILE_SCHEMA (('AUTOMOTIVE_DESIGN { 1 0 10303 214 3 1 1 }'));
ENDSEC;

DATA;
#10=MECHANICAL_DESIGN_GEOMETRIC_PRESENTATION_REPRESENTATION('',(#101),#4043);
#63=(
BOUNDED_CURVE()
B_SPLINE_CURVE(2,(#3961,#3962,#3963),.UNSPECIFIED.,.F.,.F.)
B_SPLINE_CURVE_WITH_KNOTS((3,3),(0.144988513094728,0.791574906712449),
 .UNSPECIFIED.)
CURVE()
GEOMETRIC_REPRESENTATION_ITEM()
RATIONAL_B_SPLINE_CURVE((1.09282032302755,1.26188021535082,1.09282032302931))
REPRESENTATION_ITEM('')
);
#64=(
BOUNDED_CURVE()
B_SPLINE_CURVE(2,(#3965,#3966,#3967),.UNSPECIFIED.,.F.,.F.)
B_SPLINE_CURVE_WITH_KNOTS((3,3),(0.144988513094728,0.791574906712449),
 .UNSPECIFIED.)
CURVE()
GEOMETRIC_REPRESENTATION_ITEM()
RATIONAL_B_SPLINE_CURVE((1.09282032302755,1.26188021535082,1.09282032302931))
REPRESENTATION_ITEM('')
);
#65=(
BOUNDED_CURVE()
B_SPLINE_CURVE(2,(#3969,#3970,#3971),.UNSPECIFIED.,.F.,.F.)
B_SPLINE_CURVE_WITH_KNOTS((3,3),(0.144988513094728,0.791574906712449),
 .UNSPECIFIED.)
CURVE()
GEOMETRIC_REPRESENTATION_ITEM()
RATIONAL_B_SPLINE_CURVE((1.09282032302755,1.26188021535082,1.09282032302931))
REPRESENTATION_ITEM('')
);
#66=(
BOUNDED_CURVE()
B_SPLINE_CURVE(2,(#3973,#3974,#3975),.UNSPECIFIED.,.F.,.F.)
B_SPLINE_CURVE_WITH_KNOTS((3,3),(0.144988513094728,0.791574906712449),
 .UNSPECIFIED.)
CURVE()
GEOMETRIC_REPRESENTATION_ITEM()
RATIONAL_B_SPLINE_CURVE((1.09282032302755,1.26188021535082,1.09282032302931))
REPRESENTATION_ITEM('')
);
#67=(
BOUNDED_CURVE()
B_SPLINE_CURVE(2,(#3977,#3978,#3979),.UNSPECIFIED.,.F.,.F.)
B_SPLINE_CURVE_WITH_KNOTS((3,3),(0.144988513094728,0.791574906712449),
 .UNSPECIFIED.)
CURVE()
GEOMETRIC_REPRESENTATION_ITEM()
RATIONAL_B_SPLINE_CURVE((1.09282032302755,1.26188021535082,1.09282032302931))
REPRESENTATION_ITEM('')
);
#68=(
BOUNDED_CURVE()
B_SPLINE_CURVE(2,(#3980,#3981,#3982),.UNSPECIFIED.,.F.,.F.)
B_SPLINE_CURVE_WITH_KNOTS((3,3),(0.144988513094727,0.791574906712449),
 .UNSPECIFIED.)
CURVE()
GEOMETRIC_REPRESENTATION_ITEM()
RATIONAL_B_SPLINE_CURVE((1.09282032302755,1.26188021535082,1.09282032302931))
REPRESENTATION_ITEM('')
);
#74=CONICAL_SURFACE('',#2533,0.27,0.785398163397448);
#75=CONICAL_SURFACE('',#2536,0.576175134594813,1.0471975511966);
#83=SHAPE_REPRESENTATION_RELATIONSHIP('SRR','None',#4090,#91);
#91=ADVANCED_BREP_SHAPE_REPRESENTATION('',(#111),#4042);
#101=STYLED_ITEM('',(#4204),#111);
#111=MANIFOLD_SOLID_BREP('Body1',#2218);
#152=FACE_BOUND('',#529,.T.);
#232=PLANE('',#2535);
#233=PLANE('',#2538);
#234=PLANE('',#2539);
#235=PLANE('',#2540);
#236=PLANE('',#2541);
#237=PLANE('',#2542);
#238=PLANE('',#2543);
#239=PLANE('',#2544);
#240=PLANE('',#2545);
#353=FACE_OUTER_BOUND('',#517,.T.);
#354=FACE_OUTER_BOUND('',#518,.T.);
#355=FACE_OUTER_BOUND('',#519,.T.);
#356=FACE_OUTER_BOUND('',#520,.T.);
#357=FACE_OUTER_BOUND('',#521,.T.);
#358=FACE_OUTER_BOUND('',#522,.T.);
#359=FACE_OUTER_BOUND('',#523,.T.);
#360=FACE_OUTER_BOUND('',#524,.T.);
#361=FACE_OUTER_BOUND('',#525,.T.);
#362=FACE_OUTER_BOUND('',#526,.T.);
#363=FACE_OUTER_BOUND('',#527,.T.);
#364=FACE_OUTER_BOUND('',#528,.T.);
#517=EDGE_LOOP('',(#1995,#1996,#1997,#1998));
#518=EDGE_LOOP('',(#1999,#2000,#2001,#2002));
#519=EDGE_LOOP('',(#2003));
#520=EDGE_LOOP('',(#2004,#2005,#2006,#2007,#2008,#2009,#2010,#2011,#2012));
#521=EDGE_LOOP('',(#2013,#2014,#2015,#2016));
#522=EDGE_LOOP('',(#2017,#2018,#2019,#2020));
#523=EDGE_LOOP('',(#2021,#2022,#2023,#2024));
#524=EDGE_LOOP('',(#2025,#2026,#2027,#2028));
#525=EDGE_LOOP('',(#2029,#2030,#2031,#2032));
#526=EDGE_LOOP('',(#2033,#2034,#2035,#2036));
#527=EDGE_LOOP('',(#2037));
#528=EDGE_LOOP('',(#2038,#2039,#2040,#2041,#2042,#2043));
#529=EDGE_LOOP('',(#2044));
#630=CIRCLE('',#2531,0.2942);
#631=CIRCLE('',#2532,0.2942);
#632=CIRCLE('',#2534,0.24);
#633=CIRCLE('',#2537,0.475);
#790=LINE('',#3948,#961);
#791=LINE('',#3953,#962);
#792=LINE('',#3959,#963);
#793=LINE('',#3985,#964);
#794=LINE('',#3987,#965);
#795=LINE('',#3988,#966);
#796=LINE('',#3991,#967);
#797=LINE('',#3992,#968);
#798=LINE('',#3995,#969);
#799=LINE('',#3996,#970);
#800=LINE('',#3999,#971);
#801=LINE('',#4000,#972);
#802=LINE('',#4003,#973);
#803=LINE('',#4004,#974);
#804=LINE('',#4006,#975);
#961=VECTOR('',#3163,0.3);
#962=VECTOR('',#3170,0.27);
#963=VECTOR('',#3177,0.576175134594813);
#964=VECTOR('',#3180,1.);
#965=VECTOR('',#3181,1.);
#966=VECTOR('',#3182,1.);
#967=VECTOR('',#3185,1.);
#968=VECTOR('',#3186,1.);
#969=VECTOR('',#3189,1.);
#970=VECTOR('',#3190,1.);
#971=VECTOR('',#3193,1.);
#972=VECTOR('',#3194,1.);
#973=VECTOR('',#3197,1.);
#974=VECTOR('',#3198,1.);
#975=VECTOR('',#3201,1.);
#1153=VERTEX_POINT('',#3945);
#1154=VERTEX_POINT('',#3947);
#1155=VERTEX_POINT('',#3951);
#1156=VERTEX_POINT('',#3956);
#1157=VERTEX_POINT('',#3958);
#1158=VERTEX_POINT('',#3960);
#1159=VERTEX_POINT('',#3964);
#1160=VERTEX_POINT('',#3968);
#1161=VERTEX_POINT('',#3972);
#1162=VERTEX_POINT('',#3976);
#1163=VERTEX_POINT('',#3984);
#1164=VERTEX_POINT('',#3986);
#1165=VERTEX_POINT('',#3990);
#1166=VERTEX_POINT('',#3994);
#1167=VERTEX_POINT('',#3998);
#1168=VERTEX_POINT('',#4002);
#1436=EDGE_CURVE('',#1153,#1153,#630,.F.);
#1437=EDGE_CURVE('',#1153,#1154,#790,.T.);
#1438=EDGE_CURVE('',#1154,#1154,#631,.F.);
#1439=EDGE_CURVE('',#1155,#1155,#632,.T.);
#1440=EDGE_CURVE('',#1155,#1153,#791,.T.);
#1441=EDGE_CURVE('',#1156,#1156,#633,.T.);
#1442=EDGE_CURVE('',#1156,#1157,#792,.T.);
#1443=EDGE_CURVE('',#1158,#1157,#63,.T.);
#1444=EDGE_CURVE('',#1159,#1158,#64,.T.);
#1445=EDGE_CURVE('',#1160,#1159,#65,.T.);
#1446=EDGE_CURVE('',#1161,#1160,#66,.T.);
#1447=EDGE_CURVE('',#1162,#1161,#67,.T.);
#1448=EDGE_CURVE('',#1157,#1162,#68,.T.);
#1449=EDGE_CURVE('',#1163,#1161,#793,.T.);
#1450=EDGE_CURVE('',#1163,#1164,#794,.T.);
#1451=EDGE_CURVE('',#1164,#1162,#795,.T.);
#1452=EDGE_CURVE('',#1165,#1160,#796,.T.);
#1453=EDGE_CURVE('',#1165,#1163,#797,.T.);
#1454=EDGE_CURVE('',#1166,#1159,#798,.T.);
#1455=EDGE_CURVE('',#1166,#1165,#799,.T.);
#1456=EDGE_CURVE('',#1167,#1158,#800,.T.);
#1457=EDGE_CURVE('',#1167,#1166,#801,.T.);
#1458=EDGE_CURVE('',#1168,#1157,#802,.T.);
#1459=EDGE_CURVE('',#1168,#1167,#803,.T.);
#1460=EDGE_CURVE('',#1164,#1168,#804,.T.);
#1995=ORIENTED_EDGE('',*,*,#1436,.F.);
#1996=ORIENTED_EDGE('',*,*,#1437,.T.);
#1997=ORIENTED_EDGE('',*,*,#1438,.F.);
#1998=ORIENTED_EDGE('',*,*,#1437,.F.);
#1999=ORIENTED_EDGE('',*,*,#1439,.F.);
#2000=ORIENTED_EDGE('',*,*,#1440,.T.);
#2001=ORIENTED_EDGE('',*,*,#1436,.T.);
#2002=ORIENTED_EDGE('',*,*,#1440,.F.);
#2003=ORIENTED_EDGE('',*,*,#1439,.T.);
#2004=ORIENTED_EDGE('',*,*,#1441,.F.);
#2005=ORIENTED_EDGE('',*,*,#1442,.T.);
#2006=ORIENTED_EDGE('',*,*,#1443,.F.);
#2007=ORIENTED_EDGE('',*,*,#1444,.F.);
#2008=ORIENTED_EDGE('',*,*,#1445,.F.);
#2009=ORIENTED_EDGE('',*,*,#1446,.F.);
#2010=ORIENTED_EDGE('',*,*,#1447,.F.);
#2011=ORIENTED_EDGE('',*,*,#1448,.F.);
#2012=ORIENTED_EDGE('',*,*,#1442,.F.);
#2013=ORIENTED_EDGE('',*,*,#1447,.T.);
#2014=ORIENTED_EDGE('',*,*,#1449,.F.);
#2015=ORIENTED_EDGE('',*,*,#1450,.T.);
#2016=ORIENTED_EDGE('',*,*,#1451,.T.);
#2017=ORIENTED_EDGE('',*,*,#1446,.T.);
#2018=ORIENTED_EDGE('',*,*,#1452,.F.);
#2019=ORIENTED_EDGE('',*,*,#1453,.T.);
#2020=ORIENTED_EDGE('',*,*,#1449,.T.);
#2021=ORIENTED_EDGE('',*,*,#1445,.T.);
#2022=ORIENTED_EDGE('',*,*,#1454,.F.);
#2023=ORIENTED_EDGE('',*,*,#1455,.T.);
#2024=ORIENTED_EDGE('',*,*,#1452,.T.);
#2025=ORIENTED_EDGE('',*,*,#1444,.T.);
#2026=ORIENTED_EDGE('',*,*,#1456,.F.);
#2027=ORIENTED_EDGE('',*,*,#1457,.T.);
#2028=ORIENTED_EDGE('',*,*,#1454,.T.);
#2029=ORIENTED_EDGE('',*,*,#1443,.T.);
#2030=ORIENTED_EDGE('',*,*,#1458,.F.);
#2031=ORIENTED_EDGE('',*,*,#1459,.T.);
#2032=ORIENTED_EDGE('',*,*,#1456,.T.);
#2033=ORIENTED_EDGE('',*,*,#1448,.T.);
#2034=ORIENTED_EDGE('',*,*,#1451,.F.);
#2035=ORIENTED_EDGE('',*,*,#1460,.T.);
#2036=ORIENTED_EDGE('',*,*,#1458,.T.);
#2037=ORIENTED_EDGE('',*,*,#1441,.T.);
#2038=ORIENTED_EDGE('',*,*,#1455,.F.);
#2039=ORIENTED_EDGE('',*,*,#1457,.F.);
#2040=ORIENTED_EDGE('',*,*,#1459,.F.);
#2041=ORIENTED_EDGE('',*,*,#1460,.F.);
#2042=ORIENTED_EDGE('',*,*,#1450,.F.);
#2043=ORIENTED_EDGE('',*,*,#1453,.F.);
#2044=ORIENTED_EDGE('',*,*,#1438,.T.);
#2084=CYLINDRICAL_SURFACE('',#2530,0.2942);
#2197=ADVANCED_FACE('',(#353),#2084,.T.);
#2198=ADVANCED_FACE('',(#354),#74,.T.);
#2199=ADVANCED_FACE('',(#355),#232,.T.);
#2200=ADVANCED_FACE('',(#356),#75,.T.);
#2201=ADVANCED_FACE('',(#357),#233,.T.);
#2202=ADVANCED_FACE('',(#358),#234,.T.);
#2203=ADVANCED_FACE('',(#359),#235,.T.);
#2204=ADVANCED_FACE('',(#360),#236,.T.);
#2205=ADVANCED_FACE('',(#361),#237,.T.);
#2206=ADVANCED_FACE('',(#362),#238,.T.);
#2207=ADVANCED_FACE('',(#363),#239,.T.);
#2208=ADVANCED_FACE('',(#364,#152),#240,.F.);
#2218=CLOSED_SHELL('',(#2197,#2198,#2199,#2200,#2201,#2202,#2203,#2204,
#2205,#2206,#2207,#2208));
#2529=AXIS2_PLACEMENT_3D('',#3943,#3157,#3158);
#2530=AXIS2_PLACEMENT_3D('',#3944,#3159,#3160);
#2531=AXIS2_PLACEMENT_3D('',#3946,#3161,#3162);
#2532=AXIS2_PLACEMENT_3D('',#3949,#3164,#3165);
#2533=AXIS2_PLACEMENT_3D('',#3950,#3166,#3167);
#2534=AXIS2_PLACEMENT_3D('',#3952,#3168,#3169);
#2535=AXIS2_PLACEMENT_3D('',#3954,#3171,#3172);
#2536=AXIS2_PLACEMENT_3D('',#3955,#3173,#3174);
#2537=AXIS2_PLACEMENT_3D('',#3957,#3175,#3176);
#2538=AXIS2_PLACEMENT_3D('',#3983,#3178,#3179);
#2539=AXIS2_PLACEMENT_3D('',#3989,#3183,#3184);
#2540=AXIS2_PLACEMENT_3D('',#3993,#3187,#3188);
#2541=AXIS2_PLACEMENT_3D('',#3997,#3191,#3192);
#2542=AXIS2_PLACEMENT_3D('',#4001,#3195,#3196);
#2543=AXIS2_PLACEMENT_3D('',#4005,#3199,#3200);
#2544=AXIS2_PLACEMENT_3D('',#4007,#3202,#3203);
#2545=AXIS2_PLACEMENT_3D('',#4008,#3204,#3205);
#3157=DIRECTION('axis',(0.,0.,1.));
#3158=DIRECTION('refdir',(1.,0.,0.));
#3159=DIRECTION('center_axis',(0.,-1.,0.));
#3160=DIRECTION('ref_axis',(1.,0.,0.));
#3161=DIRECTION('center_axis',(0.,1.,0.));
#3162=DIRECTION('ref_axis',(1.,0.,0.));
#3163=DIRECTION('',(0.,1.,0.));
#3164=DIRECTION('center_axis',(0.,-1.,0.));
#3165=DIRECTION('ref_axis',(1.,0.,0.));
#3166=DIRECTION('center_axis',(0.,1.,0.));
#3167=DIRECTION('ref_axis',(1.,0.,0.));
#3168=DIRECTION('center_axis',(0.,-1.,0.));
#3169=DIRECTION('ref_axis',(1.,0.,0.));
#3170=DIRECTION('',(-0.707106781186547,0.707106781186548,-8.65956056235493E-17));
#3171=DIRECTION('center_axis',(0.,-1.,0.));
#3172=DIRECTION('ref_axis',(0.,0.,-1.));
#3173=DIRECTION('center_axis',(0.,-1.,0.));
#3174=DIRECTION('ref_axis',(1.,0.,0.));
#3175=DIRECTION('center_axis',(0.,1.,0.));
#3176=DIRECTION('ref_axis',(1.,0.,0.));
#3177=DIRECTION('',(-0.866025403784439,-0.5,-1.06057523872491E-16));
#3178=DIRECTION('center_axis',(1.92296268638356E-16,0.,-1.));
#3179=DIRECTION('ref_axis',(-1.,0.,-1.92296268638356E-16));
#3180=DIRECTION('',(0.,1.,0.));
#3181=DIRECTION('',(-1.,0.,-1.92296268638356E-16));
#3182=DIRECTION('',(0.,1.,0.));
#3183=DIRECTION('center_axis',(0.866025403784439,0.,-0.5));
#3184=DIRECTION('ref_axis',(-0.5,0.,-0.866025403784439));
#3185=DIRECTION('',(0.,1.,0.));
#3186=DIRECTION('',(-0.5,0.,-0.866025403784439));
#3187=DIRECTION('center_axis',(0.866025403784439,0.,0.5));
#3188=DIRECTION('ref_axis',(0.5,0.,-0.866025403784439));
#3189=DIRECTION('',(0.,1.,0.));
#3190=DIRECTION('',(0.5,0.,-0.866025403784439));
#3191=DIRECTION('center_axis',(-1.92296268638356E-16,0.,1.));
#3192=DIRECTION('ref_axis',(1.,0.,1.92296268638356E-16));
#3193=DIRECTION('',(0.,1.,0.));
#3194=DIRECTION('',(1.,0.,1.92296268638356E-16));
#3195=DIRECTION('center_axis',(-0.866025403784439,0.,0.5));
#3196=DIRECTION('ref_axis',(0.5,0.,0.866025403784439));
#3197=DIRECTION('',(0.,1.,0.));
#3198=DIRECTION('',(0.5,0.,0.866025403784439));
#3199=DIRECTION('center_axis',(-0.866025403784439,0.,-0.5));
#3200=DIRECTION('ref_axis',(-0.5,0.,0.866025403784439));
#3201=DIRECTION('',(-0.5,0.,0.866025403784438));
#3202=DIRECTION('center_axis',(0.,1.,0.));
#3203=DIRECTION('ref_axis',(0.,0.,1.));
#3204=DIRECTION('center_axis',(0.,1.,0.));
#3205=DIRECTION('ref_axis',(1.,0.,0.));
#3943=CARTESIAN_POINT('',(0.,0.,0.));
#3944=CARTESIAN_POINT('Origin',(0.,-1.445,0.));
#3945=CARTESIAN_POINT('',(-0.2942,-2.9458,3.60291088309151E-17));
#3946=CARTESIAN_POINT('Origin',(0.,-2.9458,0.));
#3947=CARTESIAN_POINT('',(-0.2942,0.,-3.60291088309151E-17));
#3948=CARTESIAN_POINT('',(-0.2942,-1.445,-3.60291088309151E-17));
#3949=CARTESIAN_POINT('Origin',(0.,0.,0.));
#3950=CARTESIAN_POINT('Origin',(0.,-2.97,0.));
#3951=CARTESIAN_POINT('',(-0.24,-3.,-2.93915231795365E-17));
#3952=CARTESIAN_POINT('Origin',(0.,-3.,0.));
#3953=CARTESIAN_POINT('',(-0.27,-2.97,-3.30654635769785E-17));
#3954=CARTESIAN_POINT('Origin',(0.,-3.,0.));
#3955=CARTESIAN_POINT('Origin',(0.,0.341586508806388,0.));
#3956=CARTESIAN_POINT('',(-0.475,0.4,-5.81707229594993E-17));
#3957=CARTESIAN_POINT('Origin',(0.,0.4,0.));
#3958=CARTESIAN_POINT('',(-0.577350269189626,0.340908044531739,-7.07050159149938E-17));
#3959=CARTESIAN_POINT('',(-0.576175134594813,0.341586508806388,-7.05611034329833E-17));
#3960=CARTESIAN_POINT('',(-0.288675134594813,0.340908044531739,0.5));
#3961=CARTESIAN_POINT('Ctrl Pts',(-0.288675134594813,0.340908044531739,
0.5));
#3962=CARTESIAN_POINT('Ctrl Pts',(-0.433012701893303,0.424241377863696,
0.249999999998124));
#3963=CARTESIAN_POINT('Ctrl Pts',(-0.577350269189626,0.340908044531739,
-7.07050159149938E-17));
#3964=CARTESIAN_POINT('',(0.288675134594813,0.340908044531739,0.5));
#3965=CARTESIAN_POINT('Ctrl Pts',(0.288675134594813,0.340908044531739,0.5));
#3966=CARTESIAN_POINT('Ctrl Pts',(-2.16648921025353E-12,0.424241377863696,
0.5));
#3967=CARTESIAN_POINT('Ctrl Pts',(-0.288675134594813,0.340908044531739,
0.5));
#3968=CARTESIAN_POINT('',(0.577350269189626,0.340908044531739,0.));
#3969=CARTESIAN_POINT('Ctrl Pts',(0.577350269189626,0.340908044531739,0.));
#3970=CARTESIAN_POINT('Ctrl Pts',(0.433012701891136,0.424241377863697,0.250000000001876));
#3971=CARTESIAN_POINT('Ctrl Pts',(0.288675134594813,0.340908044531739,0.5));
#3972=CARTESIAN_POINT('',(0.288675134594813,0.340908044531739,-0.5));
#3973=CARTESIAN_POINT('Ctrl Pts',(0.288675134594813,0.340908044531739,-0.5));
#3974=CARTESIAN_POINT('Ctrl Pts',(0.433012701893303,0.424241377863696,-0.249999999998124));
#3975=CARTESIAN_POINT('Ctrl Pts',(0.577350269189626,0.340908044531739,0.));
#3976=CARTESIAN_POINT('',(-0.288675134594813,0.340908044531739,-0.5));
#3977=CARTESIAN_POINT('Ctrl Pts',(-0.288675134594813,0.340908044531739,
-0.5));
#3978=CARTESIAN_POINT('Ctrl Pts',(2.16660023255599E-12,0.424241377863696,
-0.5));
#3979=CARTESIAN_POINT('Ctrl Pts',(0.288675134594813,0.340908044531739,-0.5));
#3980=CARTESIAN_POINT('Ctrl Pts',(-0.577350269189626,0.340908044531739,
-7.07050159149938E-17));
#3981=CARTESIAN_POINT('Ctrl Pts',(-0.433012701891136,0.424241377863697,
-0.250000000001876));
#3982=CARTESIAN_POINT('Ctrl Pts',(-0.288675134594813,0.340908044531739,
-0.5));
#3983=CARTESIAN_POINT('Origin',(0.288675134594813,0.,-0.5));
#3984=CARTESIAN_POINT('',(0.288675134594813,0.,-0.5));
#3985=CARTESIAN_POINT('',(0.288675134594813,0.,-0.5));
#3986=CARTESIAN_POINT('',(-0.288675134594813,0.,-0.5));
#3987=CARTESIAN_POINT('',(0.288675134594813,0.,-0.5));
#3988=CARTESIAN_POINT('',(-0.288675134594813,0.,-0.5));
#3989=CARTESIAN_POINT('Origin',(0.577350269189626,0.,0.));
#3990=CARTESIAN_POINT('',(0.577350269189626,0.,0.));
#3991=CARTESIAN_POINT('',(0.577350269189626,0.,0.));
#3992=CARTESIAN_POINT('',(0.577350269189626,0.,0.));
#3993=CARTESIAN_POINT('Origin',(0.288675134594813,0.,0.5));
#3994=CARTESIAN_POINT('',(0.288675134594813,0.,0.5));
#3995=CARTESIAN_POINT('',(0.288675134594813,0.,0.5));
#3996=CARTESIAN_POINT('',(0.288675134594813,0.,0.5));
#3997=CARTESIAN_POINT('Origin',(-0.288675134594813,0.,0.5));
#3998=CARTESIAN_POINT('',(-0.288675134594813,0.,0.5));
#3999=CARTESIAN_POINT('',(-0.288675134594813,0.,0.5));
#4000=CARTESIAN_POINT('',(-0.288675134594813,0.,0.5));
#4001=CARTESIAN_POINT('Origin',(-0.577350269189626,0.,-7.07050159149938E-17));
#4002=CARTESIAN_POINT('',(-0.577350269189626,0.,-7.07050159149938E-17));
#4003=CARTESIAN_POINT('',(-0.577350269189626,0.,-7.07050159149938E-17));
#4004=CARTESIAN_POINT('',(-0.577350269189626,0.,-7.07050159149938E-17));
#4005=CARTESIAN_POINT('Origin',(-0.288675134594813,0.,-0.5));
#4006=CARTESIAN_POINT('',(-0.288675134594813,0.,-0.5));
#4007=CARTESIAN_POINT('Origin',(0.,0.4,0.));
#4008=CARTESIAN_POINT('Origin',(0.,0.,0.));
#4031=UNCERTAINTY_MEASURE_WITH_UNIT(LENGTH_MEASURE(0.001),#4044,
'DISTANCE_ACCURACY_VALUE',
'Maximum model space distance between geometric entities at asserted c
onnectivities');
#4032=UNCERTAINTY_MEASURE_WITH_UNIT(LENGTH_MEASURE(0.001),#4044,
'DISTANCE_ACCURACY_VALUE',
'Maximum model space distance between geometric entities at asserted c
onnectivities');
#4042=(
GEOMETRIC_REPRESENTATION_CONTEXT(3)
GLOBAL_UNCERTAINTY_ASSIGNED_CONTEXT((#4031))
GLOBAL_UNIT_ASSIGNED_CONTEXT((#4044,#4046,#4047))
REPRESENTATION_CONTEXT('','3D')
);
#4043=(
GEOMETRIC_REPRESENTATION_CONTEXT(3)
GLOBAL_UNCERTAINTY_ASSIGNED_CONTEXT((#4032))
GLOBAL_UNIT_ASSIGNED_CONTEXT((#4044,#4046,#4047))
REPRESENTATION_CONTEXT('','3D')
);
#4044=(
LENGTH_UNIT()
NAMED_UNIT(*)
SI_UNIT(.CENTI.,.METRE.)
);
#4046=(
NAMED_UNIT(*)
PLANE_ANGLE_UNIT()
SI_UNIT($,.RADIAN.)
);
#4047=(
NAMED_UNIT(*)
SI_UNIT($,.STERADIAN.)
SOLID_ANGLE_UNIT()
);
#4057=SHAPE_DEFINITION_REPRESENTATION(#4067,#4090);
#4067=PRODUCT_DEFINITION_SHAPE('',$,#4101);
#4090=SHAPE_REPRESENTATION('',(#2529),#4042);
#4091=PRODUCT_DEFINITION_CONTEXT('part definition',#4123,'design');
#4101=PRODUCT_DEFINITION('Hex Bolt - M6 x 30 mm',
'Hex Bolt - M6 x 30 mm',#4111,#4091);
#4111=PRODUCT_DEFINITION_FORMATION('',$,#4134);
#4123=APPLICATION_CONTEXT(
'Core Data for Automotive Mechanical Design Process');
#4124=PRODUCT_CONTEXT('part definition',#4123,'mechanical');
#4134=PRODUCT('Hex Bolt - M6 x 30 mm','Hex Bolt - M6 x 30 mm',
'Hex Bolt - M6 x 30 mm',(#4124));
#4198=COLOUR_RGB('Black',0.12,0.14,0.17);
#4199=FILL_AREA_STYLE_COLOUR('',#4198);
#4200=FILL_AREA_STYLE('',(#4199));
#4201=SURFACE_STYLE_FILL_AREA(#4200);
#4202=SURFACE_SIDE_STYLE('',(#4201));
#4203=SURFACE_STYLE_USAGE(.BOTH.,#4202);
#4204=PRESENTATION_STYLE_ASSIGNMENT((#4203));
ENDSEC;
END-ISO-10303-21;
